ISO-10303-21;
HEADER;
FILE_DESCRIPTION (('STEP AP203'),
    '1' );
FILE_NAME ('Hook Pin_Varsayılan.step',
    '2026-10-08T23:54:15',
    ( '' ),
    ( '' ),
    'SwSTEP 2.0',
    'SolidWorks 2024',
    '' );
FILE_SCHEMA (( 'AUTOMOTIVE_DESIGN' ));
ENDSEC;

DATA;
#81=CIRCLE ( 'NONE', #97288, 2.000000000000001776 ) ;
#508=ADVANCED_BREP_SHAPE_REPRESENTATION ( '', ( #42246, #37391 ), #19636 ) ;
#1493=CYLINDRICAL_SURFACE ( 'NONE', #93750, 2.000000000000001776 ) ;
#1533=CARTESIAN_POINT ( 'NONE',  ( 0.000000000000000000, 0.000000000000000000, 0.000000000000000000 ) ) ;
#2607=DIRECTION ( 'NONE',  ( -1.000000000000000000, 0.000000000000000000, -0.000000000000000000 ) ) ;
#3950=DIRECTION ( 'NONE',  ( -0.000000000000000000, -1.000000000000000000, -0.000000000000000000 ) ) ;
#4824=CARTESIAN_POINT ( 'NONE',  ( 21.57151214508649772, 3.625915217019311583E-15, -1.699999999999999956 ) ) ;
#5096=EDGE_CURVE ( 'NONE', #42079, #42444, #43208, .T. ) ;
#5828=LINE ( 'NONE', #37777, #39160 ) ;
#5933=CARTESIAN_POINT ( 'NONE',  ( 21.57151214508649772, 3.625915217019311583E-15, -1.699999999999999956 ) ) ;
#5951=EDGE_LOOP ( 'NONE', ( #79420, #80661, #90756, #6867 ) ) ;
#6026=VERTEX_POINT ( 'NONE', #51325 ) ;
#6867=ORIENTED_EDGE ( 'NONE', *, *, #34132, .F. ) ;
#6942=DIRECTION ( 'NONE',  ( 1.000000000000000000, 0.000000000000000000, 0.000000000000000000 ) ) ;
#7130=TOROIDAL_SURFACE ( 'NONE', #34672, 1.049999999999998934, 0.5999999999999999778 ) ;
#8035=AXIS2_PLACEMENT_3D ( 'NONE', #50072, #42468, #28217 ) ;
#8053=CYLINDRICAL_SURFACE ( 'NONE', #19072, 2.000000000000001776 ) ;
#8164=ORIENTED_EDGE ( 'NONE', *, *, #48385, .T. ) ;
#8263=AXIS2_PLACEMENT_3D ( 'NONE', #99627, #46361, #54982 ) ;
#8391=ORIENTED_EDGE ( 'NONE', *, *, #18085, .F. ) ;
#9196=CARTESIAN_POINT ( 'NONE',  ( 21.57151214508649772, 3.625915217019311583E-15, 0.000000000000000000 ) ) ;
#9975=DIRECTION ( 'NONE',  ( 0.000000000000000000, 0.000000000000000000, -1.000000000000000000 ) ) ;
#10054=DIRECTION ( 'NONE',  ( -1.000000000000000000, 0.000000000000000000, 0.000000000000000000 ) ) ;
#10624=DIRECTION ( 'NONE',  ( -1.000000000000000000, 0.000000000000000000, -0.000000000000000000 ) ) ;
#10922=ORIENTED_EDGE ( 'NONE', *, *, #89695, .T. ) ;
#11010=ORIENTED_EDGE ( 'NONE', *, *, #76556, .T. ) ;
#11571=CIRCLE ( 'NONE', #24529, 1.500000000000001332 ) ;
#12323=DIRECTION ( 'NONE',  ( 0.000000000000000000, 0.000000000000000000, -1.000000000000000000 ) ) ;
#12413=CARTESIAN_POINT ( 'NONE',  ( 21.57151214508649772, 3.625915217019311583E-15, -1.700000000000000178 ) ) ;
#12427=CYLINDRICAL_SURFACE ( 'NONE', #65835, 1.500000000000001332 ) ;
#12723=VERTEX_POINT ( 'NONE', #45767 ) ;
#12769=ORIENTED_EDGE ( 'NONE', *, *, #82424, .T. ) ;
#12931=DIRECTION ( 'NONE',  ( -0.000000000000000000, -0.000000000000000000, 1.000000000000000000 ) ) ;
#13849=CIRCLE ( 'NONE', #26836, 1.649999999999998579 ) ;
#14488=DIRECTION ( 'NONE',  ( 0.000000000000000000, 0.000000000000000000, -1.000000000000000000 ) ) ;
#14552=ORIENTED_EDGE ( 'NONE', *, *, #82424, .F. ) ;
#15273=DIRECTION ( 'NONE',  ( 0.000000000000000000, 0.000000000000000000, -1.000000000000000000 ) ) ;
#15852=ADVANCED_FACE ( 'NONE', ( #57407, #65028 ), #78690, .F. ) ;
#16510=PRODUCT_DEFINITION_FORMATION_WITH_SPECIFIED_SOURCE ( 'ANY', '', #63584, .NOT_KNOWN. ) ;
#18085=EDGE_CURVE ( 'NONE', #47977, #12723, #75478, .T. ) ;
#18544=FACE_OUTER_BOUND ( 'NONE', #82706, .T. ) ;
#19072=AXIS2_PLACEMENT_3D ( 'NONE', #39002, #93280, #10054 ) ;
#19451=CARTESIAN_POINT ( 'NONE',  ( 21.57151214508649772, 3.625915217019311583E-15, 0.5000000000000000000 ) ) ;
#19527=CARTESIAN_POINT ( 'NONE',  ( 23.22151214508649986, 3.827981938878625524E-15, -1.699999999999999956 ) ) ;
#19636=( GEOMETRIC_REPRESENTATION_CONTEXT ( 3 ) GLOBAL_UNCERTAINTY_ASSIGNED_CONTEXT ( ( #37787 ) ) GLOBAL_UNIT_ASSIGNED_CONTEXT ( ( #19934, #20423, #28063 ) ) REPRESENTATION_CONTEXT ( 'NONE', 'WORKASPACE' ) );
#19932=CARTESIAN_POINT ( 'NONE',  ( 19.92151214508649915, 3.625915217019311583E-15, -1.699999999999999956 ) ) ;
#19934=( LENGTH_UNIT ( ) NAMED_UNIT ( * ) SI_UNIT ( .MILLI., .METRE. ) );
#20073=AXIS2_PLACEMENT_3D ( 'NONE', #5933, #67853, #83553 ) ;
#20423=( NAMED_UNIT ( * ) PLANE_ANGLE_UNIT ( ) SI_UNIT ( $, .RADIAN. ) );
#21101=CARTESIAN_POINT ( 'NONE',  ( 21.57151214508649772, 3.625915217019311583E-15, -1.699999999999999956 ) ) ;
#21434=ORIENTED_EDGE ( 'NONE', *, *, #67093, .F. ) ;
#23003=CARTESIAN_POINT ( 'NONE',  ( 23.57151214508650128, 3.870844576848782668E-15, 0.5000000000000000000 ) ) ;
#23355=VERTEX_POINT ( 'NONE', #34703 ) ;
#23397=CARTESIAN_POINT ( 'NONE',  ( 21.57151214508649772, 3.625915217019311583E-15, -2.299999999999999822 ) ) ;
#23634=ADVANCED_FACE ( 'NONE', ( #88251, #57322 ), #61540, .F. ) ;
#23996=DIRECTION ( 'NONE',  ( 1.000000000000000000, 0.000000000000000000, 0.000000000000000000 ) ) ;
#24497=DIRECTION ( 'NONE',  ( -0.000000000000000000, -0.000000000000000000, -1.000000000000000000 ) ) ;
#24529=AXIS2_PLACEMENT_3D ( 'NONE', #82451, #74833, #60636 ) ;
#24854=DIRECTION ( 'NONE',  ( 1.000000000000000000, 0.000000000000000000, 0.000000000000000000 ) ) ;
#26836=AXIS2_PLACEMENT_3D ( 'NONE', #77666, #15273, #68079 ) ;
#27282=DIRECTION ( 'NONE',  ( 0.000000000000000000, 0.000000000000000000, -1.000000000000000000 ) ) ;
#27582=DIRECTION ( 'NONE',  ( 0.000000000000000000, 0.000000000000000000, 1.000000000000000000 ) ) ;
#27629=ORIENTED_EDGE ( 'NONE', *, *, #89079, .F. ) ;
#27669=AXIS2_PLACEMENT_3D ( 'NONE', #31731, #62697, #71804 ) ;
#27827=FACE_OUTER_BOUND ( 'NONE', #5951, .T. ) ;
#27942=AXIS2_PLACEMENT_3D ( 'NONE', #91176, #36897, #6942 ) ;
#28063=( NAMED_UNIT ( * ) SI_UNIT ( $, .STERADIAN. ) SOLID_ANGLE_UNIT ( ) );
#28217=DIRECTION ( 'NONE',  ( 1.000000000000000000, 0.000000000000000000, 0.000000000000000000 ) ) ;
#28256=ORIENTED_EDGE ( 'NONE', *, *, #58106, .T. ) ;
#28648=DIRECTION ( 'NONE',  ( 0.000000000000000000, 0.000000000000000000, -1.000000000000000000 ) ) ;
#29298=CARTESIAN_POINT ( 'NONE',  ( 22.62151214508649844, 3.791242534904204664E-15, -2.299999999999999822 ) ) ;
#29596=ORIENTED_EDGE ( 'NONE', *, *, #32113, .F. ) ;
#29849=ORIENTED_EDGE ( 'NONE', *, *, #55639, .F. ) ;
#30849=PRODUCT_DEFINITION ( 'UNKNOWN', '', #16510, #82459 ) ;
#31261=AXIS2_PLACEMENT_3D ( 'NONE', #23397, #54383, #2607 ) ;
#31731=CARTESIAN_POINT ( 'NONE',  ( 21.57151214508649772, 3.625915217019311583E-15, -2.299999999999999822 ) ) ;
#32063=EDGE_CURVE ( 'NONE', #47977, #6026, #5828, .T. ) ;
#32113=EDGE_CURVE ( 'NONE', #6026, #34128, #11571, .T. ) ;
#32371=CIRCLE ( 'NONE', #61569, 0.5999999999999998668 ) ;
#32483=DIRECTION ( 'NONE',  ( -0.000000000000000000, -0.000000000000000000, -1.000000000000000000 ) ) ;
#33541=EDGE_CURVE ( 'NONE', #56728, #23355, #37640, .T. ) ;
#34128=VERTEX_POINT ( 'NONE', #89675 ) ;
#34132=EDGE_CURVE ( 'NONE', #42079, #23355, #32371, .T. ) ;
#34283=DIRECTION ( 'NONE',  ( 1.000000000000000000, 0.000000000000000000, 0.000000000000000000 ) ) ;
#34672=AXIS2_PLACEMENT_3D ( 'NONE', #75481, #73508, #50672 ) ;
#34703=CARTESIAN_POINT ( 'NONE',  ( 20.52151214508650057, 3.625915217019311583E-15, -2.299999999999999822 ) ) ;
#35477=CLOSED_SHELL ( 'NONE', ( #49721, #58920, #64736, #63365, #50121, #15852, #39918, #44385, #23634, #42486 ) ) ;
#35596=APPLICATION_CONTEXT ( 'configuration controlled 3d designs of mechanical parts and assemblies' ) ;
#35950=EDGE_CURVE ( 'NONE', #23355, #56728, #71421, .T. ) ;
#36233=ORIENTED_EDGE ( 'NONE', *, *, #89695, .F. ) ;
#36456=EDGE_LOOP ( 'NONE', ( #39560, #65587, #8164, #43309 ) ) ;
#36680=PLANE ( 'NONE',  #76791 ) ;
#36886=CYLINDRICAL_SURFACE ( 'NONE', #20073, 1.500000000000001332 ) ;
#36897=DIRECTION ( 'NONE',  ( 0.000000000000000000, 0.000000000000000000, 1.000000000000000000 ) ) ;
#37276=SHAPE_DEFINITION_REPRESENTATION ( #95185, #91803 ) ;
#37311=EDGE_LOOP ( 'NONE', ( #14552, #8391, #58801, #75527 ) ) ;
#37391=AXIS2_PLACEMENT_3D ( 'NONE', #1533, #63447, #24854 ) ;
#37463=ORIENTED_EDGE ( 'NONE', *, *, #48385, .F. ) ;
#37640=CIRCLE ( 'NONE', #50620, 1.049999999999998934 ) ;
#37777=CARTESIAN_POINT ( 'NONE',  ( 23.07151214508650128, 3.625915217019311583E-15, -1.699999999999999956 ) ) ;
#37787=UNCERTAINTY_MEASURE_WITH_UNIT (LENGTH_MEASURE( 1.000000000000000082E-05 ), #19934, 'distance_accuracy_value', 'NONE');
#38138=PLANE ( 'NONE',  #31261 ) ;
#38743=LINE ( 'NONE', #23003, #65293 ) ;
#39002=CARTESIAN_POINT ( 'NONE',  ( 21.57151214508649772, 3.625915217019311583E-15, 0.5000000000000000000 ) ) ;
#39160=VECTOR ( 'NONE', #12931, 1000.000000000000000 ) ;
#39560=ORIENTED_EDGE ( 'NONE', *, *, #76556, .F. ) ;
#39645=CARTESIAN_POINT ( 'NONE',  ( 19.57151214508649772, 3.625915217019311583E-15, 0.000000000000000000 ) ) ;
#39918=ADVANCED_FACE ( 'NONE', ( #53128 ), #36886, .T. ) ;
#40043=FACE_OUTER_BOUND ( 'NONE', #92229, .T. ) ;
#40886=CARTESIAN_POINT ( 'NONE',  ( 20.07151214508649772, 3.809612236891415094E-15, -1.699999999999999956 ) ) ;
#40929=DIRECTION ( 'NONE',  ( -1.000000000000000000, 0.000000000000000000, 0.000000000000000000 ) ) ;
#41904=DIRECTION ( 'NONE',  ( -0.000000000000000000, -0.000000000000000000, 1.000000000000000000 ) ) ;
#42079=VERTEX_POINT ( 'NONE', #19932 ) ;
#42088=DIRECTION ( 'NONE',  ( 0.000000000000000000, 0.000000000000000000, -1.000000000000000000 ) ) ;
#42246=MANIFOLD_SOLID_BREP ( 'Radyus1', #35477 ) ;
#42444=VERTEX_POINT ( 'NONE', #19527 ) ;
#42468=DIRECTION ( 'NONE',  ( 0.000000000000000000, 0.000000000000000000, 1.000000000000000000 ) ) ;
#42486=ADVANCED_FACE ( 'NONE', ( #97652 ), #96208, .T. ) ;
#43208=CIRCLE ( 'NONE', #99885, 1.649999999999998579 ) ;
#43309=ORIENTED_EDGE ( 'NONE', *, *, #55639, .T. ) ;
#44287=VERTEX_POINT ( 'NONE', #39645 ) ;
#44385=ADVANCED_FACE ( 'NONE', ( #92922 ), #38138, .T. ) ;
#45767=CARTESIAN_POINT ( 'NONE',  ( 20.07151214508649772, 3.809612236891415094E-15, -1.699999999999999956 ) ) ;
#46361=DIRECTION ( 'NONE',  ( -1.224646799147353207E-16, 1.000000000000000000, 0.000000000000000000 ) ) ;
#46412=ORIENTED_EDGE ( 'NONE', *, *, #33541, .T. ) ;
#46665=DIRECTION ( 'NONE',  ( -0.000000000000000000, -0.000000000000000000, -1.000000000000000000 ) ) ;
#46945=AXIS2_PLACEMENT_3D ( 'NONE', #69685, #24497, #23996 ) ;
#47165=DIRECTION ( 'NONE',  ( -1.000000000000000000, 0.000000000000000000, 0.000000000000000000 ) ) ;
#47977=VERTEX_POINT ( 'NONE', #87384 ) ;
#48385=EDGE_CURVE ( 'NONE', #74504, #44287, #63456, .T. ) ;
#49704=CARTESIAN_POINT ( 'NONE',  ( 21.57151214508649772, 3.625915217019311583E-15, -1.699999999999999956 ) ) ;
#49721=ADVANCED_FACE ( 'NONE', ( #27827 ), #7130, .T. ) ;
#50072=CARTESIAN_POINT ( 'NONE',  ( 21.57151214508649772, 3.625915217019311583E-15, 0.5000000000000000000 ) ) ;
#50121=ADVANCED_FACE ( 'NONE', ( #88982 ), #36680, .T. ) ;
#50620=AXIS2_PLACEMENT_3D ( 'NONE', #79841, #12323, #95573 ) ;
#50672=DIRECTION ( 'NONE',  ( -1.000000000000000000, 0.000000000000000000, 0.000000000000000000 ) ) ;
#51325=CARTESIAN_POINT ( 'NONE',  ( 23.07151214508650128, 3.625915217019311583E-15, 0.000000000000000000 ) ) ;
#52170=ORIENTED_EDGE ( 'NONE', *, *, #92605, .F. ) ;
#53128=FACE_OUTER_BOUND ( 'NONE', #37311, .T. ) ;
#53744=FACE_OUTER_BOUND ( 'NONE', #36456, .T. ) ;
#53799=VERTEX_POINT ( 'NONE', #90719 ) ;
#54015=VECTOR ( 'NONE', #32483, 1000.000000000000000 ) ;
#54383=DIRECTION ( 'NONE',  ( 0.000000000000000000, 0.000000000000000000, -1.000000000000000000 ) ) ;
#54982=DIRECTION ( 'NONE',  ( -1.000000000000000000, -1.224646799147353207E-16, 0.000000000000000000 ) ) ;
#55639=EDGE_CURVE ( 'NONE', #44287, #64682, #78112, .T. ) ;
#55836=CARTESIAN_POINT ( 'NONE',  ( 21.57151214508649772, 3.625915217019311583E-15, -1.699999999999999956 ) ) ;
#56031=AXIS2_PLACEMENT_3D ( 'NONE', #49704, #42088, #10624 ) ;
#56343=DIRECTION ( 'NONE',  ( -1.000000000000000000, 0.000000000000000000, 0.000000000000000000 ) ) ;
#56728=VERTEX_POINT ( 'NONE', #29298 ) ;
#56903=DIRECTION ( 'NONE',  ( 0.000000000000000000, 0.000000000000000000, 1.000000000000000000 ) ) ;
#57322=FACE_OUTER_BOUND ( 'NONE', #91688, .T. ) ;
#57407=FACE_BOUND ( 'NONE', #69395, .T. ) ;
#57574=CIRCLE ( 'NONE', #83468, 2.000000000000001776 ) ;
#58106=EDGE_CURVE ( 'NONE', #42444, #42079, #13849, .T. ) ;
#58330=CIRCLE ( 'NONE', #93941, 1.500000000000001332 ) ;
#58476=CIRCLE ( 'NONE', #8263, 0.5999999999999998668 ) ;
#58621=MECHANICAL_CONTEXT ( 'NONE', #92623, 'mechanical' ) ;
#58652=DIRECTION ( 'NONE',  ( 0.000000000000000000, 0.000000000000000000, 1.000000000000000000 ) ) ;
#58801=ORIENTED_EDGE ( 'NONE', *, *, #32063, .T. ) ;
#58920=ADVANCED_FACE ( 'NONE', ( #18544 ), #12427, .T. ) ;
#59404=EDGE_LOOP ( 'NONE', ( #75767, #95768 ) ) ;
#60200=EDGE_LOOP ( 'NONE', ( #72524, #88370 ) ) ;
#60636=DIRECTION ( 'NONE',  ( 1.000000000000000000, 0.000000000000000000, 0.000000000000000000 ) ) ;
#60690=DIRECTION ( 'NONE',  ( -1.000000000000000000, 0.000000000000000000, 0.000000000000000000 ) ) ;
#61540=PLANE ( 'NONE',  #56031 ) ;
#61569=AXIS2_PLACEMENT_3D ( 'NONE', #88184, #3950, #27282 ) ;
#62697=DIRECTION ( 'NONE',  ( 0.000000000000000000, 0.000000000000000000, -1.000000000000000000 ) ) ;
#63365=ADVANCED_FACE ( 'NONE', ( #53744 ), #8053, .T. ) ;
#63447=DIRECTION ( 'NONE',  ( 0.000000000000000000, 0.000000000000000000, 1.000000000000000000 ) ) ;
#63456=LINE ( 'NONE', #70545, #54015 ) ;
#63584=PRODUCT ( 'Hook Pin_Varsay\X2\0131\X0\lan', 'Hook Pin_Varsay\X2\0131\X0\lan', '', ( #58621 ) ) ;
#64682=VERTEX_POINT ( 'NONE', #78582 ) ;
#64736=ADVANCED_FACE ( 'NONE', ( #40043 ), #1493, .T. ) ;
#65028=FACE_OUTER_BOUND ( 'NONE', #85747, .T. ) ;
#65293=VECTOR ( 'NONE', #92530, 1000.000000000000000 ) ;
#65587=ORIENTED_EDGE ( 'NONE', *, *, #98562, .F. ) ;
#65826=AXIS2_PLACEMENT_3D ( 'NONE', #79488, #9975, #40929 ) ;
#65835=AXIS2_PLACEMENT_3D ( 'NONE', #4824, #41904, #34283 ) ;
#67093=EDGE_CURVE ( 'NONE', #64682, #44287, #57574, .T. ) ;
#67154=DIRECTION ( 'NONE',  ( 1.000000000000000000, 0.000000000000000000, -0.000000000000000000 ) ) ;
#67853=DIRECTION ( 'NONE',  ( -0.000000000000000000, -0.000000000000000000, 1.000000000000000000 ) ) ;
#68079=DIRECTION ( 'NONE',  ( -1.000000000000000000, 0.000000000000000000, 0.000000000000000000 ) ) ;
#68650=DIRECTION ( 'NONE',  ( 1.000000000000000000, 0.000000000000000000, 0.000000000000000000 ) ) ;
#69395=EDGE_LOOP ( 'NONE', ( #29596, #36233 ) ) ;
#69685=CARTESIAN_POINT ( 'NONE',  ( 21.57151214508649772, 3.625915217019311583E-15, 0.000000000000000000 ) ) ;
#70337=LINE ( 'NONE', #40886, #72385 ) ;
#70545=CARTESIAN_POINT ( 'NONE',  ( 19.57151214508649772, 3.625915217019311583E-15, 0.5000000000000000000 ) ) ;
#71120=EDGE_LOOP ( 'NONE', ( #82613, #28256, #98324, #81586 ) ) ;
#71421=CIRCLE ( 'NONE', #27669, 1.049999999999998934 ) ;
#71804=DIRECTION ( 'NONE',  ( -1.000000000000000000, 0.000000000000000000, 0.000000000000000000 ) ) ;
#71908=ORIENTED_EDGE ( 'NONE', *, *, #32063, .F. ) ;
#72006=CARTESIAN_POINT ( 'NONE',  ( 21.57151214508649772, 3.625915217019311583E-15, 0.5000000000000000000 ) ) ;
#72385=VECTOR ( 'NONE', #87056, 1000.000000000000000 ) ;
#72524=ORIENTED_EDGE ( 'NONE', *, *, #18085, .T. ) ;
#72752=EDGE_CURVE ( 'NONE', #42444, #56728, #58476, .T. ) ;
#73508=DIRECTION ( 'NONE',  ( 0.000000000000000000, 0.000000000000000000, -1.000000000000000000 ) ) ;
#73533=AXIS2_PLACEMENT_3D ( 'NONE', #12413, #28648, #99139 ) ;
#74504=VERTEX_POINT ( 'NONE', #81327 ) ;
#74536=CIRCLE ( 'NONE', #46945, 1.500000000000001332 ) ;
#74750=DIRECTION ( 'NONE',  ( 0.000000000000000000, 0.000000000000000000, 1.000000000000000000 ) ) ;
#74833=DIRECTION ( 'NONE',  ( -0.000000000000000000, -0.000000000000000000, -1.000000000000000000 ) ) ;
#75201=AXIS2_PLACEMENT_3D ( 'NONE', #9196, #56903, #87324 ) ;
#75478=CIRCLE ( 'NONE', #65826, 1.500000000000001332 ) ;
#75481=CARTESIAN_POINT ( 'NONE',  ( 21.57151214508649772, 3.625915217019311583E-15, -1.700000000000000178 ) ) ;
#75527=ORIENTED_EDGE ( 'NONE', *, *, #32113, .T. ) ;
#75739=CARTESIAN_POINT ( 'NONE',  ( 21.57151214508649772, 3.625915217019311583E-15, 0.000000000000000000 ) ) ;
#75767=ORIENTED_EDGE ( 'NONE', *, *, #98562, .T. ) ;
#76556=EDGE_CURVE ( 'NONE', #53799, #64682, #38743, .T. ) ;
#76791=AXIS2_PLACEMENT_3D ( 'NONE', #19451, #27582, #67154 ) ;
#77666=CARTESIAN_POINT ( 'NONE',  ( 21.57151214508649772, 3.625915217019311583E-15, -1.699999999999999956 ) ) ;
#78112=CIRCLE ( 'NONE', #27942, 2.000000000000001776 ) ;
#78582=CARTESIAN_POINT ( 'NONE',  ( 23.57151214508650128, 3.870844576848782668E-15, 0.000000000000000000 ) ) ;
#78690=PLANE ( 'NONE',  #75201 ) ;
#79420=ORIENTED_EDGE ( 'NONE', *, *, #5096, .T. ) ;
#79488=CARTESIAN_POINT ( 'NONE',  ( 21.57151214508649772, 3.625915217019311583E-15, -1.699999999999999956 ) ) ;
#79788=ORIENTED_EDGE ( 'NONE', *, *, #35950, .T. ) ;
#79841=CARTESIAN_POINT ( 'NONE',  ( 21.57151214508649772, 3.625915217019311583E-15, -2.299999999999999822 ) ) ;
#80661=ORIENTED_EDGE ( 'NONE', *, *, #72752, .T. ) ;
#81327=CARTESIAN_POINT ( 'NONE',  ( 19.57151214508649772, 3.625915217019311583E-15, 0.5000000000000000000 ) ) ;
#81493=DIRECTION ( 'NONE',  ( 1.000000000000000000, 0.000000000000000000, 0.000000000000000000 ) ) ;
#81586=ORIENTED_EDGE ( 'NONE', *, *, #33541, .F. ) ;
#82337=SHAPE_REPRESENTATION_RELATIONSHIP ( 'NONE' , 'NONE' ,  #91803, #508 ) ;
#82424=EDGE_CURVE ( 'NONE', #12723, #34128, #70337, .T. ) ;
#82451=CARTESIAN_POINT ( 'NONE',  ( 21.57151214508649772, 3.625915217019311583E-15, 0.000000000000000000 ) ) ;
#82459=DESIGN_CONTEXT ( 'detailed design', #35596, 'design' ) ;
#82613=ORIENTED_EDGE ( 'NONE', *, *, #72752, .F. ) ;
#82706=EDGE_LOOP ( 'NONE', ( #27629, #12769, #10922, #71908 ) ) ;
#83468=AXIS2_PLACEMENT_3D ( 'NONE', #75739, #74750, #68650 ) ;
#83553=DIRECTION ( 'NONE',  ( 1.000000000000000000, 0.000000000000000000, 0.000000000000000000 ) ) ;
#85747=EDGE_LOOP ( 'NONE', ( #29849, #21434 ) ) ;
#85828=CIRCLE ( 'NONE', #8035, 2.000000000000001776 ) ;
#87056=DIRECTION ( 'NONE',  ( -0.000000000000000000, -0.000000000000000000, 1.000000000000000000 ) ) ;
#87242=ORIENTED_EDGE ( 'NONE', *, *, #67093, .T. ) ;
#87324=DIRECTION ( 'NONE',  ( 1.000000000000000000, 0.000000000000000000, -0.000000000000000000 ) ) ;
#87384=CARTESIAN_POINT ( 'NONE',  ( 23.07151214508650128, 3.625915217019311583E-15, -1.699999999999999956 ) ) ;
#88184=CARTESIAN_POINT ( 'NONE',  ( 20.52151214508650057, 3.625915217019311583E-15, -1.700000000000000178 ) ) ;
#88251=FACE_BOUND ( 'NONE', #60200, .T. ) ;
#88370=ORIENTED_EDGE ( 'NONE', *, *, #89079, .T. ) ;
#88982=FACE_OUTER_BOUND ( 'NONE', #59404, .T. ) ;
#89079=EDGE_CURVE ( 'NONE', #12723, #47977, #58330, .T. ) ;
#89675=CARTESIAN_POINT ( 'NONE',  ( 20.07151214508649772, 3.809612236891415094E-15, 0.000000000000000000 ) ) ;
#89695=EDGE_CURVE ( 'NONE', #34128, #6026, #74536, .T. ) ;
#90719=CARTESIAN_POINT ( 'NONE',  ( 23.57151214508650128, 3.870844576848782668E-15, 0.5000000000000000000 ) ) ;
#90756=ORIENTED_EDGE ( 'NONE', *, *, #35950, .F. ) ;
#91176=CARTESIAN_POINT ( 'NONE',  ( 21.57151214508649772, 3.625915217019311583E-15, 0.000000000000000000 ) ) ;
#91688=EDGE_LOOP ( 'NONE', ( #91971, #100176 ) ) ;
#91803=SHAPE_REPRESENTATION ( 'Hook Pin_Varsay\X2\0131\X0\lan', ( #37391 ), #19636 ) ;
#91971=ORIENTED_EDGE ( 'NONE', *, *, #5096, .F. ) ;
#92229=EDGE_LOOP ( 'NONE', ( #52170, #11010, #87242, #37463 ) ) ;
#92530=DIRECTION ( 'NONE',  ( -0.000000000000000000, -0.000000000000000000, -1.000000000000000000 ) ) ;
#92605=EDGE_CURVE ( 'NONE', #53799, #74504, #85828, .T. ) ;
#92623=APPLICATION_CONTEXT ( 'configuration controlled 3d designs of mechanical parts and assemblies' ) ;
#92922=FACE_OUTER_BOUND ( 'NONE', #96617, .T. ) ;
#93280=DIRECTION ( 'NONE',  ( -0.000000000000000000, -0.000000000000000000, -1.000000000000000000 ) ) ;
#93750=AXIS2_PLACEMENT_3D ( 'NONE', #72006, #46665, #47165 ) ;
#93941=AXIS2_PLACEMENT_3D ( 'NONE', #55836, #94873, #56343 ) ;
#94873=DIRECTION ( 'NONE',  ( 0.000000000000000000, 0.000000000000000000, -1.000000000000000000 ) ) ;
#95185=PRODUCT_DEFINITION_SHAPE ( 'NONE', 'NONE',  #30849 ) ;
#95573=DIRECTION ( 'NONE',  ( -1.000000000000000000, 0.000000000000000000, 0.000000000000000000 ) ) ;
#95768=ORIENTED_EDGE ( 'NONE', *, *, #92605, .T. ) ;
#96208=TOROIDAL_SURFACE ( 'NONE', #73533, 1.049999999999998934, 0.5999999999999999778 ) ;
#96617=EDGE_LOOP ( 'NONE', ( #79788, #46412 ) ) ;
#97288=AXIS2_PLACEMENT_3D ( 'NONE', #98193, #58652, #81493 ) ;
#97652=FACE_OUTER_BOUND ( 'NONE', #71120, .T. ) ;
#98193=CARTESIAN_POINT ( 'NONE',  ( 21.57151214508649772, 3.625915217019311583E-15, 0.5000000000000000000 ) ) ;
#98324=ORIENTED_EDGE ( 'NONE', *, *, #34132, .T. ) ;
#98562=EDGE_CURVE ( 'NONE', #74504, #53799, #81, .T. ) ;
#99139=DIRECTION ( 'NONE',  ( -1.000000000000000000, 0.000000000000000000, 0.000000000000000000 ) ) ;
#99627=CARTESIAN_POINT ( 'NONE',  ( 22.62151214508649844, 3.754503130929783804E-15, -1.700000000000000178 ) ) ;
#99885=AXIS2_PLACEMENT_3D ( 'NONE', #21101, #14488, #60690 ) ;
#100176=ORIENTED_EDGE ( 'NONE', *, *, #58106, .F. ) ;
#100469=COLOUR_RGB('Black', 0.09019608, 0.27058824, 0.51372549);
#100470=FILL_AREA_STYLE_COLOUR('',#100469);
#100471=FILL_AREA_STYLE('',(#100470));
#100472=SURFACE_STYLE_FILL_AREA(#100471);
#100473=SURFACE_SIDE_STYLE('',(#100472));
#100474=SURFACE_STYLE_USAGE(.BOTH.,#100473);
#100475=PRESENTATION_STYLE_ASSIGNMENT((#100474));
#100476=STYLED_ITEM('',(#100475),#42246);
#100477=MECHANICAL_DESIGN_GEOMETRIC_PRESENTATION_REPRESENTATION('',(#100476),#19636);
ENDSEC;
END-ISO-10303-21;
